ISO-10303-21;
HEADER;
FILE_DESCRIPTION (('STEP AP203'),
    '1' );
FILE_NAME ('Blade_Predeterminado.step',
    '2026-10-08T11:28:20',
    ( '' ),
    ( '' ),
    'SwSTEP 2.0',
    'SolidWorks 2024',
    '' );
FILE_SCHEMA (( 'AUTOMOTIVE_DESIGN' ));
ENDSEC;

DATA;
#39=ORIENTED_EDGE ( 'NONE', *, *, #8561, .F. ) ;
#81=APPLICATION_CONTEXT ( 'configuration controlled 3d designs of mechanical parts and assemblies' ) ;
#85=CIRCLE ( 'NONE', #9462, 0.4999999999999865663 ) ;
#88=CARTESIAN_POINT ( 'NONE',  ( -0.3675725891509493137, 0.000000000000000000, -0.3389548520155291622 ) ) ;
#94=ORIENTED_EDGE ( 'NONE', *, *, #15196, .T. ) ;
#100=AXIS2_PLACEMENT_3D ( 'NONE', #7008, #14909, #675 ) ;
#151=DIRECTION ( 'NONE',  ( 0.000000000000000000, 1.000000000000000000, 0.000000000000000000 ) ) ;
#164=EDGE_CURVE ( 'NONE', #10316, #6640, #6443, .T. ) ;
#222=DIRECTION ( 'NONE',  ( 0.000000000000000000, 0.000000000000000000, 1.000000000000000000 ) ) ;
#282=DIRECTION ( 'NONE',  ( 0.000000000000000000, 1.000000000000000000, 0.000000000000000000 ) ) ;
#296=SHAPE_DEFINITION_REPRESENTATION ( #8175, #10891 ) ;
#453=DIRECTION ( 'NONE',  ( 0.000000000000000000, -0.000000000000000000, 1.000000000000000000 ) ) ;
#551=CARTESIAN_POINT ( 'NONE',  ( 29.71057115341584165, 0.000000000000000000, 36.39324188472025412 ) ) ;
#555=EDGE_CURVE ( 'NONE', #12741, #14503, #11276, .T. ) ;
#615=ORIENTED_EDGE ( 'NONE', *, *, #2812, .F. ) ;
#675=DIRECTION ( 'NONE',  ( 0.000000000000000000, 0.000000000000000000, -1.000000000000000000 ) ) ;
#688=VERTEX_POINT ( 'NONE', #88 ) ;
#752=CARTESIAN_POINT ( 'NONE',  ( 3.800081604575823224, 1.749999999999317213, 48.85836690712316255 ) ) ;
#765=ORIENTED_EDGE ( 'NONE', *, *, #6856, .T. ) ;
#773=CIRCLE ( 'NONE', #6696, 0.5000000000000018874 ) ;
#783=ORIENTED_EDGE ( 'NONE', *, *, #6545, .F. ) ;
#824=ORIENTED_EDGE ( 'NONE', *, *, #13683, .T. ) ;
#829=CARTESIAN_POINT ( 'NONE',  ( 25.37742002255717466, 1.750000000000000000, 70.49803269364883818 ) ) ;
#841=ORIENTED_EDGE ( 'NONE', *, *, #9714, .T. ) ;
#879=APPLICATION_CONTEXT ( 'configuration controlled 3d designs of mechanical parts and assemblies' ) ;
#886=CARTESIAN_POINT ( 'NONE',  ( 30.50390178861119139, 1.750000000002257083, 35.39815044914973186 ) ) ;
#918=ADVANCED_FACE ( 'NONE', ( #1933 ), #6818, .T. ) ;
#922=VERTEX_POINT ( 'NONE', #7572 ) ;
#945=CARTESIAN_POINT ( 'NONE',  ( 3.586150740732019226, 2.099999999999147438, 48.99645249886114584 ) ) ;
#948=CARTESIAN_POINT ( 'NONE',  ( 26.30339064689345463, 0.000000000000000000, 68.98786334397659914 ) ) ;
#958=CARTESIAN_POINT ( 'NONE',  ( 46.59046791724578895, 0.000000000000000000, 61.03149078395468763 ) ) ;
#963=ORIENTED_EDGE ( 'NONE', *, *, #9785, .F. ) ;
#985=CONICAL_SURFACE ( 'NONE', #15311, 0.5000000000000004441, 0.6283185307179600665 ) ;
#1010=DIRECTION ( 'NONE',  ( 0.000000000000000000, 1.000000000000000000, 0.000000000000000000 ) ) ;
#1023=CARTESIAN_POINT ( 'NONE',  ( -5.011228476432583179, 0.000000000000000000, 8.417957015065626436 ) ) ;
#1036=PLANE ( 'NONE',  #13106 ) ;
#1046=PRODUCT_DEFINITION ( 'UNKNOWN', '', #10666, #4186 ) ;
#1085=CARTESIAN_POINT ( 'NONE',  ( 46.59046791724578895, 1.632027846198980036E-15, 61.03149078395468763 ) ) ;
#1097=CARTESIAN_POINT ( 'NONE',  ( -7.119039342394801295, 2.100000000000745715, 20.68784477908849340 ) ) ;
#1110=EDGE_CURVE ( 'NONE', #10252, #14298, #4559, .T. ) ;
#1112=EDGE_CURVE ( 'NONE', #5602, #8895, #4401, .T. ) ;
#1114=DIRECTION ( 'NONE',  ( 0.000000000000000000, 1.000000000000000000, 0.000000000000000000 ) ) ;
#1115=CARTESIAN_POINT ( 'NONE',  ( 39.66138262230233380, 2.099999999999999645, 42.07085476361616116 ) ) ;
#1143=CARTESIAN_POINT ( 'NONE',  ( 52.73038795364751508, 1.750000000000000000, 69.25342193720584305 ) ) ;
#1162=CARTESIAN_POINT ( 'NONE',  ( 30.32986759126112730, 0.7500000000000000000, 41.04214087805579680 ) ) ;
#1194=CARTESIAN_POINT ( 'NONE',  ( 7.113306724408225534, 2.331468351713773494E-16, 51.45871142768356066 ) ) ;
#1227=CARTESIAN_POINT ( 'NONE',  ( 38.58381714758451864, 1.749999999999999778, 41.14817863027235489 ) ) ;
#1238=DIRECTION ( 'NONE',  ( 0.000000000000000000, 0.000000000000000000, -1.000000000000000000 ) ) ;
#1240=EDGE_CURVE ( 'NONE', #6640, #10252, #1332, .T. ) ;
#1249=ORIENTED_EDGE ( 'NONE', *, *, #5177, .T. ) ;
#1266=CARTESIAN_POINT ( 'NONE',  ( 30.32986759126112730, 0.000000000000000000, 45.04214087805580391 ) ) ;
#1332=CIRCLE ( 'NONE', #7085, 0.5000000000000004441 ) ;
#1337=CARTESIAN_POINT ( 'NONE',  ( 1.635615696801046015, 1.750000000000000000, -0.6802899045268993028 ) ) ;
#1419=( LENGTH_UNIT ( ) NAMED_UNIT ( * ) SI_UNIT ( .MILLI., .METRE. ) );
#1430=CARTESIAN_POINT ( 'NONE',  ( 23.12860366745965734, 2.331468351712828833E-16, 67.62772795920155033 ) ) ;
#1439=DIRECTION ( 'NONE',  ( 0.000000000000000000, 0.000000000000000000, 1.000000000000000000 ) ) ;
#1502=ORIENTED_EDGE ( 'NONE', *, *, #5053, .F. ) ;
#1560=EDGE_LOOP ( 'NONE', ( #3843, #13117, #4746, #11499 ) ) ;
#1565=CARTESIAN_POINT ( 'NONE',  ( 10.02369947906852232, 1.750000000002257083, 14.18264983478496966 ) ) ;
#1602=AXIS2_PLACEMENT_3D ( 'NONE', #8066, #14029, #3425 ) ;
#1606=CARTESIAN_POINT ( 'NONE',  ( -6.807027589832401304, 1.750000000000027311, 11.03434205495325848 ) ) ;
#1640=CARTESIAN_POINT ( 'NONE',  ( 26.28048204801264731, 0.000000000000000000, 69.48733826436532013 ) ) ;
#1667=CARTESIAN_POINT ( 'NONE',  ( 0.000000000000000000, 1.750000000000000000, 0.000000000000000000 ) ) ;
#1732=CARTESIAN_POINT ( 'NONE',  ( 12.01748009419283925, 2.331468351711883680E-16, 57.58516622398010298 ) ) ;
#1741=CIRCLE ( 'NONE', #6426, 2.000000000000001776 ) ;
#1764=VERTEX_POINT ( 'NONE', #14616 ) ;
#1784=CARTESIAN_POINT ( 'NONE',  ( 23.10845500747044667, 2.100000000000000089, 28.62577620913018706 ) ) ;
#1862=CARTESIAN_POINT ( 'NONE',  ( 30.32986759126112730, 0.7500000000000000000, 43.04214087805580391 ) ) ;
#1865=CARTESIAN_POINT ( 'NONE',  ( 1.870406778884745380, 2.100000000000000089, -0.7779448751454841604 ) ) ;
#1910=CARTESIAN_POINT ( 'NONE',  ( -1.885054460532284537, 1.750000000000027311, 38.35079268139701014 ) ) ;
#1924=ADVANCED_FACE ( 'NONE', ( #14923 ), #2216, .F. ) ;
#1933=FACE_OUTER_BOUND ( 'NONE', #12198, .T. ) ;
#1956=ORIENTED_EDGE ( 'NONE', *, *, #8954, .F. ) ;
#1962=EDGE_LOOP ( 'NONE', ( #7380, #5824, #14934, #1994 ) ) ;
#1994=ORIENTED_EDGE ( 'NONE', *, *, #2538, .F. ) ;
#1997=CONICAL_SURFACE ( 'NONE', #3218, 1.000000000000000888, 0.6283185307179600665 ) ;
#2031=EDGE_CURVE ( 'NONE', #2235, #688, #15022, .T. ) ;
#2065=AXIS2_PLACEMENT_3D ( 'NONE', #15040, #9366, #9448 ) ;
#2075=VECTOR ( 'NONE', #11847, 1000.000000000000227 ) ;
#2086=CARTESIAN_POINT ( 'NONE',  ( 51.62524086895222553, 0.000000000000000000, 69.88209797381236399 ) ) ;
#2123=CARTESIAN_POINT ( 'NONE',  ( 43.47613484165132292, 2.100000000006494449, 51.22794247056654626 ) ) ;
#2170=ORIENTED_EDGE ( 'NONE', *, *, #2031, .T. ) ;
#2180=CARTESIAN_POINT ( 'NONE',  ( -0.7212374594705488473, 0.000000000000000000, 37.83387651873656665 ) ) ;
#2195=DIRECTION ( 'NONE',  ( 0.000000000000000000, 0.000000000000000000, -1.000000000000000000 ) ) ;
#2204=CARTESIAN_POINT ( 'NONE',  ( -1.873266413721881518, 2.331468351712828833E-16, 1.481691765633328606 ) ) ;
#2216=CYLINDRICAL_SURFACE ( 'NONE', #6031, 3.500000000000003109 ) ;
#2220=CIRCLE ( 'NONE', #4688, 2.000000000000001776 ) ;
#2235=VERTEX_POINT ( 'NONE', #12293 ) ;
#2259=CARTESIAN_POINT ( 'NONE',  ( 25.24449781760964129, 2.100000000000000089, 70.71481607157352300 ) ) ;
#2274=CARTESIAN_POINT ( 'NONE',  ( 38.25296960060443752, 0.000000000000000000, 42.65758570601111188 ) ) ;
#2328=AXIS2_PLACEMENT_3D ( 'NONE', #11887, #151, #222 ) ;
#2349=FACE_BOUND ( 'NONE', #12167, .T. ) ;
#2361=CARTESIAN_POINT ( 'NONE',  ( -0.7212374594705489583, 2.331468351712828340E-16, 37.83387651873656665 ) ) ;
#2370=FACE_BOUND ( 'NONE', #4813, .T. ) ;
#2373=ORIENTED_EDGE ( 'NONE', *, *, #4618, .F. ) ;
#2403=CARTESIAN_POINT ( 'NONE',  ( -4.488583703910701495, 2.100000000000000089, 2.894752896148880428 ) ) ;
#2405=CARTESIAN_POINT ( 'NONE',  ( 47.72094894359807427, 1.749999999998650191, 60.44734918181273997 ) ) ;
#2429=ADVANCED_FACE ( 'NONE', ( #6647 ), #5937, .T. ) ;
#2447=EDGE_LOOP ( 'NONE', ( #15060, #8323, #15035, #4487, #11630, #11580, #12081, #7847, #824, #765 ) ) ;
#2479=CARTESIAN_POINT ( 'NONE',  ( 0.000000000000000000, 0.000000000000000000, 0.000000000000000000 ) ) ;
#2506=CARTESIAN_POINT ( 'NONE',  ( 51.19063959271458231, 0.000000000000000000, 70.62932606827693860 ) ) ;
#2513=EDGE_LOOP ( 'NONE', ( #6314, #3750 ) ) ;
#2538=EDGE_CURVE ( 'NONE', #14191, #13258, #11772, .T. ) ;
#2576=CARTESIAN_POINT ( 'NONE',  ( 5.133649534803208070, 1.750000000002257083, 6.659653797658318553 ) ) ;
#2587=CARTESIAN_POINT ( 'NONE',  ( 30.32986759126112730, 1.750000000000000000, 41.04214087805579680 ) ) ;
#2595=EDGE_CURVE ( 'NONE', #5598, #3495, #9611, .T. ) ;
#2667=EDGE_LOOP ( 'NONE', ( #14522, #9827, #12242, #13187 ) ) ;
#2684=CARTESIAN_POINT ( 'NONE',  ( -2.157807494669262027, 1.750000000000239142, -0.2731155010785480952 ) ) ;
#2710=CARTESIAN_POINT ( 'NONE',  ( 0.000000000000000000, 1.750000000000000000, 0.000000000000000000 ) ) ;
#2736=VECTOR ( 'NONE', #12235, 1000.000000000000227 ) ;
#2755=VECTOR ( 'NONE', #5893, 1000.000000000000000 ) ;
#2757=CIRCLE ( 'NONE', #2990, 1.771449424009387208 ) ;
#2812=EDGE_CURVE ( 'NONE', #922, #6135, #10003, .T. ) ;
#2863=CARTESIAN_POINT ( 'NONE',  ( 51.16773099383375012, 8.094429697821059805E-15, 70.62880098866565959 ) ) ;
#2873=CARTESIAN_POINT ( 'NONE',  ( 1.990297875723448406, 0.000000000000000000, 3.483276348926833244 ) ) ;
#2990=AXIS2_PLACEMENT_3D ( 'NONE', #2710, #7413, #7647 ) ;
#3014=ADVANCED_FACE ( 'NONE', ( #13787 ), #985, .T. ) ;
#3037=CARTESIAN_POINT ( 'NONE',  ( 0.000000000000000000, 0.000000000000000000, -0.5000000000000018874 ) ) ;
#3051=ORIENTED_EDGE ( 'NONE', *, *, #9325, .F. ) ;
#3067=CARTESIAN_POINT ( 'NONE',  ( 26.22222779830891781, 1.750000000000000000, 70.75745246403606359 ) ) ;
#3107=CARTESIAN_POINT ( 'NONE',  ( 51.19063959271458231, 0.000000000000000000, 70.62932606827693860 ) ) ;
#3126=B_SPLINE_CURVE_WITH_KNOTS ( 'NONE', 3,
 ( #14708, #12361, #10269, #13830, #5332, #3233, #10046, #7867, #10119, #14860 ),
 .UNSPECIFIED., .F., .F.,
 ( 4, 2, 2, 2, 4 ),
 ( 0.000000000000000000, 0.01436113971778546841, 0.02872227943557093682, 0.04308341915335640870, 0.05744455887114187365 ),
 .UNSPECIFIED. ) ;
#3148=LINE ( 'NONE', #6634, #10443 ) ;
#3195=EDGE_CURVE ( 'NONE', #5598, #14191, #2220, .T. ) ;
#3218=AXIS2_PLACEMENT_3D ( 'NONE', #4135, #12388, #13863 ) ;
#3233=CARTESIAN_POINT ( 'NONE',  ( 11.91826453496364380, -2.051692149507289097E-14, 18.75693026131821028 ) ) ;
#3291=EDGE_CURVE ( 'NONE', #11406, #7450, #3880, .T. ) ;
#3328=DIRECTION ( 'NONE',  ( 0.000000000000000000, 0.000000000000000000, 1.000000000000000000 ) ) ;
#3337=CARTESIAN_POINT ( 'NONE',  ( 10.87549112447535293, 2.099999999999148770, 58.60001680419858161 ) ) ;
#3340=DIRECTION ( 'NONE',  ( 0.000000000000000000, 1.000000000000000000, 0.000000000000000000 ) ) ;
#3363=CARTESIAN_POINT ( 'NONE',  ( -0.3675725891509493137, 0.000000000000000000, -0.3389548520155291622 ) ) ;
#3421=CARTESIAN_POINT ( 'NONE',  ( 47.94704514886957014, 2.100000000000000089, 60.33052086138381043 ) ) ;
#3425=DIRECTION ( 'NONE',  ( 0.000000000000000000, 0.000000000000000000, -1.000000000000000000 ) ) ;
#3434=CARTESIAN_POINT ( 'NONE',  ( -5.011228476432583179, 2.331468351712828833E-16, 8.417957015065626436 ) ) ;
#3466=DIRECTION ( 'NONE',  ( -0.000000000000000000, 1.000000000000000000, -0.000000000000000000 ) ) ;
#3467=ORIENTED_EDGE ( 'NONE', *, *, #10014, .T. ) ;
#3490=VECTOR ( 'NONE', #8042, 1000.000000000000000 ) ;
#3495=VERTEX_POINT ( 'NONE', #1266 ) ;
#3514=ORIENTED_EDGE ( 'NONE', *, *, #5177, .F. ) ;
#3546=ORIENTED_EDGE ( 'NONE', *, *, #6856, .F. ) ;
#3568=CARTESIAN_POINT ( 'NONE',  ( 14.67769753127737253, 0.000000000000000000, 60.42036742134819605 ) ) ;
#3616=MECHANICAL_CONTEXT ( 'NONE', #81, 'mechanical' ) ;
#3656=SHAPE_REPRESENTATION_RELATIONSHIP ( 'NONE' , 'NONE' ,  #10891, #5218 ) ;
#3665=VERTEX_POINT ( 'NONE', #11333 ) ;
#3667=LINE ( 'NONE', #10479, #2075 ) ;
#3681=CARTESIAN_POINT ( 'NONE',  ( 30.32986759126112730, 0.7500000000000000000, 45.04214087805580391 ) ) ;
#3743=DIRECTION ( 'NONE',  ( -0.000000000000000000, -1.000000000000000000, -0.000000000000000000 ) ) ;
#3744=CIRCLE ( 'NONE', #13872, 3.500000000000003109 ) ;
#3750=ORIENTED_EDGE ( 'NONE', *, *, #15196, .F. ) ;
#3802=ORIENTED_EDGE ( 'NONE', *, *, #10540, .F. ) ;
#3809=CARTESIAN_POINT ( 'NONE',  ( 12.90981819559527111, 1.750000000002257083, 17.95896478634083948 ) ) ;
#3842=B_SPLINE_CURVE_WITH_KNOTS ( 'NONE', 3,
 ( #5083, #2684, #9796, #3925, #13360, #12186, #1606, #5158, #12413, #8006, #11257, #1910, #15061, #752, #11411, #14985, #4310, #15140, #10408, #829 ),
 .UNSPECIFIED., .F., .F.,
 ( 4, 2, 2, 2, 2, 2, 2, 2, 2, 4 ),
 ( 0.000000000000000000, 0.005303151365135050539, 0.01060630273027009934, 0.02121260546054020216, 0.03181890819081030497, 0.04242521092108039737, 0.05303151365135049672, 0.06363781638162059606, 0.07424411911189068847, 0.08485042184216079475 ),
 .UNSPECIFIED. ) ;
#3843=ORIENTED_EDGE ( 'NONE', *, *, #1110, .T. ) ;
#3880=LINE ( 'NONE', #10394, #11594 ) ;
#3925=CARTESIAN_POINT ( 'NONE',  ( -4.261429542763926825, 1.750000000000027756, 3.010279858880415826 ) ) ;
#3992=AXIS2_PLACEMENT_3D ( 'NONE', #15011, #11515, #8891 ) ;
#4034=CARTESIAN_POINT ( 'NONE',  ( 30.66256791564903139, 2.100000000000000089, 35.19913216203716644 ) ) ;
#4048=CIRCLE ( 'NONE', #100, 2.000000000000001776 ) ;
#4061=AXIS2_PLACEMENT_3D ( 'NONE', #4545, #11564, #13748 ) ;
#4068=CARTESIAN_POINT ( 'NONE',  ( 14.67769753127737253, 2.331468351711927067E-16, 60.42036742134819605 ) ) ;
#4095=ORIENTED_EDGE ( 'NONE', *, *, #10884, .F. ) ;
#4117=ADVANCED_FACE ( 'NONE', ( #9225 ), #11638, .T. ) ;
#4120=FACE_OUTER_BOUND ( 'NONE', #2667, .T. ) ;
#4135=CARTESIAN_POINT ( 'NONE',  ( 37.32986759126112730, 0.000000000000000000, 43.04214087805580391 ) ) ;
#4183=CARTESIAN_POINT ( 'NONE',  ( 10.22950345979100462, 2.100000000000000089, 14.03267466424344256 ) ) ;
#4186=DESIGN_CONTEXT ( 'detailed design', #879, 'design' ) ;
#4251=CYLINDRICAL_SURFACE ( 'NONE', #11181, 3.500000000000003109 ) ;
#4262=EDGE_LOOP ( 'NONE', ( #3514, #15041, #94, #5133 ) ) ;
#4310=CARTESIAN_POINT ( 'NONE',  ( 13.77177382422822838, 1.749999999999351186, 61.31538778292295433 ) ) ;
#4401=LINE ( 'NONE', #2086, #8382 ) ;
#4439=CARTESIAN_POINT ( 'NONE',  ( 52.95141737058320075, 2.100000000000000089, 69.12768672987860441 ) ) ;
#4487=ORIENTED_EDGE ( 'NONE', *, *, #5053, .T. ) ;
#4489=CARTESIAN_POINT ( 'NONE',  ( 38.25296960060453699, 0.000000000000000000, 42.65758570601131794 ) ) ;
#4511=ORIENTED_EDGE ( 'NONE', *, *, #8094, .T. ) ;
#4515=EDGE_CURVE ( 'NONE', #13423, #9221, #7516, .T. ) ;
#4522=FACE_OUTER_BOUND ( 'NONE', #1962, .T. ) ;
#4545=CARTESIAN_POINT ( 'NONE',  ( 26.28048204801264731, 0.000000000000000000, 69.48733826436532013 ) ) ;
#4559=LINE ( 'NONE', #4630, #12217 ) ;
#4579=CARTESIAN_POINT ( 'NONE',  ( -5.068140779129265638, 2.100000000000000089, 4.126857918875922238 ) ) ;
#4584=ORIENTED_EDGE ( 'NONE', *, *, #3291, .F. ) ;
#4592=FACE_OUTER_BOUND ( 'NONE', #12594, .T. ) ;
#4603=ORIENTED_EDGE ( 'NONE', *, *, #4515, .T. ) ;
#4618=EDGE_CURVE ( 'NONE', #13258, #3495, #1741, .T. ) ;
#4630=CARTESIAN_POINT ( 'NONE',  ( 26.28048204801264731, 0.000000000000000000, 69.48733826436532013 ) ) ;
#4641=DIRECTION ( 'NONE',  ( 0.4321074940959399036, -0.8090169943749466741, 0.3984653264195704980 ) ) ;
#4648=CARTESIAN_POINT ( 'NONE',  ( -5.542419796536699472, 0.000000000000000000, 11.20594165676177134 ) ) ;
#4651=DIRECTION ( 'NONE',  ( 0.000000000000000000, 0.000000000000000000, 1.000000000000000000 ) ) ;
#4674=CARTESIAN_POINT ( 'NONE',  ( -5.836568743579779728, 2.331468351712828340E-16, 17.25548782215969368 ) ) ;
#4685=CARTESIAN_POINT ( 'NONE',  ( 39.42664711868611960, 1.750000000000000000, 42.16864325401552804 ) ) ;
#4688=AXIS2_PLACEMENT_3D ( 'NONE', #15260, #13070, #4651 ) ;
#4727=CARTESIAN_POINT ( 'NONE',  ( 5.873062173554511212, 2.100000000000850964, 52.35081790185157757 ) ) ;
#4729=DIRECTION ( 'NONE',  ( 0.9989498407774402011, -0.000000000000000000, 0.04581719776161457397 ) ) ;
#4746=ORIENTED_EDGE ( 'NONE', *, *, #13250, .F. ) ;
#4792=CONICAL_SURFACE ( 'NONE', #7764, 0.5000000000000018874, 0.6283185307179600665 ) ;
#4813=EDGE_LOOP ( 'NONE', ( #12060, #11926 ) ) ;
#4891=EDGE_CURVE ( 'NONE', #13423, #688, #773, .T. ) ;
#4905=ORIENTED_EDGE ( 'NONE', *, *, #13276, .F. ) ;
#4921=FACE_OUTER_BOUND ( 'NONE', #2447, .T. ) ;
#4998=CARTESIAN_POINT ( 'NONE',  ( 0.000000000000000000, 0.000000000000000000, 0.000000000000000000 ) ) ;
#5053=EDGE_CURVE ( 'NONE', #922, #9221, #2757, .T. ) ;
#5083=CARTESIAN_POINT ( 'NONE',  ( -1.302272502657875197, 1.750000000000000000, -1.200882754745186798 ) ) ;
#5090=LINE ( 'NONE', #10031, #12684 ) ;
#5099=DIRECTION ( 'NONE',  ( 0.02693067314567074849, -0.8090169943749466741, -0.5871679841888934881 ) ) ;
#5111=CARTESIAN_POINT ( 'NONE',  ( 51.10947674412996378, 1.750000000000000000, 71.89891518833638884 ) ) ;
#5126=ADVANCED_FACE ( 'NONE', ( #9326, #2370 ), #12592, .T. ) ;
#5133=ORIENTED_EDGE ( 'NONE', *, *, #11119, .F. ) ;
#5158=CARTESIAN_POINT ( 'NONE',  ( -7.111859124059414228, 1.750000000000027311, 17.30358917253076356 ) ) ;
#5168=EDGE_LOOP ( 'NONE', ( #14812, #6461, #7756, #10351 ) ) ;
#5177=EDGE_CURVE ( 'NONE', #3665, #14114, #5460, .T. ) ;
#5206=DIRECTION ( 'NONE',  ( 0.000000000000000000, -1.000000000000000000, 0.000000000000000000 ) ) ;
#5218=ADVANCED_BREP_SHAPE_REPRESENTATION ( '', ( #12454, #9419 ), #12893 ) ;
#5230=DIRECTION ( 'NONE',  ( 0.000000000000000000, 0.000000000000000000, 1.000000000000000000 ) ) ;
#5264=CARTESIAN_POINT ( 'NONE',  ( 22.05734493763782211, 0.000000000000000000, 29.73364058993713499 ) ) ;
#5294=DIRECTION ( 'NONE',  ( 0.3072466363781645171, -0.8090169943749466741, -0.5010898195402013755 ) ) ;
#5304=DIRECTION ( 'NONE',  ( 0.000000000000000000, 1.000000000000000000, 0.000000000000000000 ) ) ;
#5332=CARTESIAN_POINT ( 'NONE',  ( 18.44985294524426322, -2.051692149507289097E-14, 26.15777747556343868 ) ) ;
#5409=CARTESIAN_POINT ( 'NONE',  ( 37.88191578704504536, 0.000000000000000000, 42.20832867525968624 ) ) ;
#5460=CIRCLE ( 'NONE', #14354, 3.500000000000003109 ) ;
#5476=DIRECTION ( 'NONE',  ( 0.000000000000000000, 0.000000000000000000, 1.000000000000000000 ) ) ;
#5510=CARTESIAN_POINT ( 'NONE',  ( 26.04203104729492679, -1.082694418179886911E-15, 69.41411580402544246 ) ) ;
#5598=VERTEX_POINT ( 'NONE', #3681 ) ;
#5602=VERTEX_POINT ( 'NONE', #1143 ) ;
#5643=DIRECTION ( 'NONE',  ( 0.000000000000000000, 1.000000000000000000, 0.000000000000000000 ) ) ;
#5649=CARTESIAN_POINT ( 'NONE',  ( -3.665378489062163236, 0.000000000000000000, 4.733462801983808532 ) ) ;
#5669=CYLINDRICAL_SURFACE ( 'NONE', #14949, 2.000000000000001776 ) ;
#5691=VECTOR ( 'NONE', #4641, 1000.000000000000000 ) ;
#5698=AXIS2_PLACEMENT_3D ( 'NONE', #7377, #282, #1439 ) ;
#5715=ORIENTED_EDGE ( 'NONE', *, *, #1112, .T. ) ;
#5728=CARTESIAN_POINT ( 'NONE',  ( -4.373225680752619304, 0.000000000000000000, 27.28944397070847927 ) ) ;
#5784=CARTESIAN_POINT ( 'NONE',  ( 26.30339064689345463, 0.000000000000000000, 68.98786334397659914 ) ) ;
#5802=CARTESIAN_POINT ( 'NONE',  ( -1.873266413721881296, 0.000000000000000000, 1.481691765633328828 ) ) ;
#5824=ORIENTED_EDGE ( 'NONE', *, *, #2595, .T. ) ;
#5870=CARTESIAN_POINT ( 'NONE',  ( 19.27433926169634049, 2.100000000000811884, 66.63156944101105239 ) ) ;
#5893=DIRECTION ( 'NONE',  ( -0.000000000000000000, -1.000000000000000000, -0.000000000000000000 ) ) ;
#5906=ADVANCED_FACE ( 'NONE', ( #2349, #4592 ), #1036, .F. ) ;
#5935=EDGE_LOOP ( 'NONE', ( #12672, #4095, #12699, #12643 ) ) ;
#5937=CONICAL_SURFACE ( 'NONE', #3992, 0.4999999999999865663, 0.6283185307179600665 ) ;
#5967=( NAMED_UNIT ( * ) PLANE_ANGLE_UNIT ( ) SI_UNIT ( $, .RADIAN. ) );
#5986=AXIS2_PLACEMENT_3D ( 'NONE', #12743, #14995, #5476 ) ;
#6031=AXIS2_PLACEMENT_3D ( 'NONE', #14050, #12577, #9330 ) ;
#6072=B_SPLINE_CURVE_WITH_KNOTS ( 'NONE', 3,
 ( #10435, #1085, #11442, #4489 ),
 .UNSPECIFIED., .F., .F.,
 ( 4, 4 ),
 ( 0.000000000000000000, 0.03035464128818402690 ),
 .UNSPECIFIED. ) ;
#6135=VERTEX_POINT ( 'NONE', #8114 ) ;
#6147=FACE_OUTER_BOUND ( 'NONE', #5168, .T. ) ;
#6168=EDGE_CURVE ( 'NONE', #3665, #14503, #12690, .T. ) ;
#6203=CIRCLE ( 'NONE', #9651, 1.771449424009387208 ) ;
#6218=EDGE_LOOP ( 'NONE', ( #4511, #4584, #4905, #5715 ) ) ;
#6223=ORIENTED_EDGE ( 'NONE', *, *, #10836, .T. ) ;
#6297=CARTESIAN_POINT ( 'NONE',  ( 26.04203104729492679, 0.000000000000000000, 69.41411580402544246 ) ) ;
#6314=ORIENTED_EDGE ( 'NONE', *, *, #555, .F. ) ;
#6361=CARTESIAN_POINT ( 'NONE',  ( 30.32986759126112730, 0.000000000000000000, 43.04214087805580391 ) ) ;
#6426=AXIS2_PLACEMENT_3D ( 'NONE', #6361, #5206, #10291 ) ;
#6435=AXIS2_PLACEMENT_3D ( 'NONE', #11281, #10273, #6643 ) ;
#6443=LINE ( 'NONE', #5510, #12771 ) ;
#6461=ORIENTED_EDGE ( 'NONE', *, *, #4891, .T. ) ;
#6463=B_SPLINE_CURVE_WITH_KNOTS ( 'NONE', 3,
 ( #3363, #12798, #2204, #6911, #14037, #3434, #8145, #4674, #8223, #12954, #10618, #2361, #11776, #7058, #1194, #1732, #4068, #7291, #1430, #6297 ),
 .UNSPECIFIED., .F., .F.,
 ( 4, 2, 2, 2, 2, 2, 2, 2, 2, 4 ),
 ( 0.000000000000000000, 0.005157128052839767690, 0.01031425610567953365, 0.02062851221135907076, 0.03094276831703860267, 0.04125702442271813458, 0.05157128052839766996, 0.06188553663407720534, 0.07219979273975672684, 0.08251404884543626916 ),
 .UNSPECIFIED. ) ;
#6493=CARTESIAN_POINT ( 'NONE',  ( 8.994679575448131459, 0.000000000000000000, 14.93252568749840137 ) ) ;
#6545=EDGE_CURVE ( 'NONE', #14298, #11802, #12188, .T. ) ;
#6597=CARTESIAN_POINT ( 'NONE',  ( 0.4616602863826347325, 7.217962787865914056E-16, -0.1920150514337511105 ) ) ;
#6634=CARTESIAN_POINT ( 'NONE',  ( 26.28048204801264731, 0.000000000000000000, 69.48733826436532013 ) ) ;
#6640=VERTEX_POINT ( 'NONE', #10271 ) ;
#6643=DIRECTION ( 'NONE',  ( 0.000000000000000000, -0.000000000000000000, 1.000000000000000000 ) ) ;
#6644=CARTESIAN_POINT ( 'NONE',  ( 0.4616602863826355096, 0.000000000000000000, -0.1920150514337429226 ) ) ;
#6647=FACE_OUTER_BOUND ( 'NONE', #8347, .T. ) ;
#6696=AXIS2_PLACEMENT_3D ( 'NONE', #2479, #11977, #1238 ) ;
#6779=EDGE_CURVE ( 'NONE', #3495, #13258, #4048, .T. ) ;
#6797=DIRECTION ( 'NONE',  ( -0.5109044416013800438, -0.8090169943749470072, 0.2906340557548426906 ) ) ;
#6818=B_SPLINE_SURFACE_WITH_KNOTS ( 'NONE', 1, 3, ( 
 ( #8889, #11133, #4034, #1784, #8739, #12445, #4183, #11212, #8963, #1865 ),
 ( #5409, #7805, #551, #5264, #8657, #13470, #6493, #12218, #2873, #6644 ) ),
 .UNSPECIFIED., .F., .F., .F.,
 ( 2, 2 ),
 ( 4, 2, 2, 2, 4 ),
 ( 0.000000000000000000, 1.000000000000000000 ),
 ( 1.315450245614885549, 1.577474171769009281, 1.839498097923133013, 2.101522024077256745, 2.363545950231380477 ),
 .UNSPECIFIED. ) ;
#6832=ORIENTED_EDGE ( 'NONE', *, *, #164, .F. ) ;
#6856=EDGE_CURVE ( 'NONE', #11095, #5602, #8737, .T. ) ;
#6909=ORIENTED_EDGE ( 'NONE', *, *, #3291, .T. ) ;
#6911=CARTESIAN_POINT ( 'NONE',  ( -3.125658737029940681, 2.331468351712828833E-16, 3.587914672538146554 ) ) ;
#6940=EDGE_CURVE ( 'NONE', #10699, #1764, #3667, .T. ) ;
#6965=CARTESIAN_POINT ( 'NONE',  ( -1.160594694320683518, 0.000000000000000000, 0.5210215923759190515 ) ) ;
#6976=CIRCLE ( 'NONE', #8483, 2.000000000000001776 ) ;
#6998=AXIS2_PLACEMENT_3D ( 'NONE', #14491, #14247, #8352 ) ;
#7008=CARTESIAN_POINT ( 'NONE',  ( 30.32986759126112730, 0.000000000000000000, 43.04214087805580391 ) ) ;
#7033=CARTESIAN_POINT ( 'NONE',  ( -2.117817860744609426, 2.099999999999999645, 38.45417591392908463 ) ) ;
#7057=ORIENTED_EDGE ( 'NONE', *, *, #1240, .T. ) ;
#7058=CARTESIAN_POINT ( 'NONE',  ( 4.869735923794942245, 2.331468351711882200E-16, 48.16793894843318924 ) ) ;
#7085=AXIS2_PLACEMENT_3D ( 'NONE', #5784, #3466, #14940 ) ;
#7100=EDGE_CURVE ( 'NONE', #688, #6640, #6463, .T. ) ;
#7101=CARTESIAN_POINT ( 'NONE',  ( 23.12860366745965734, 0.000000000000000000, 67.62772795920155033 ) ) ;
#7104=ORIENTED_EDGE ( 'NONE', *, *, #9325, .T. ) ;
#7189=ORIENTED_EDGE ( 'NONE', *, *, #8094, .F. ) ;
#7197=( NAMED_UNIT ( * ) SI_UNIT ( $, .STERADIAN. ) SOLID_ANGLE_UNIT ( ) );
#7291=CARTESIAN_POINT ( 'NONE',  ( 20.23335552821398409, 2.331468351713730107E-16, 65.44177069175029260 ) ) ;
#7316=AXIS2_PLACEMENT_3D ( 'NONE', #15030, #14010, #10367 ) ;
#7377=CARTESIAN_POINT ( 'NONE',  ( 51.19063959271458231, 1.750000000000000000, 70.12932606827693860 ) ) ;
#7380=ORIENTED_EDGE ( 'NONE', *, *, #3195, .F. ) ;
#7409=EDGE_CURVE ( 'NONE', #14191, #5598, #6976, .T. ) ;
#7413=DIRECTION ( 'NONE',  ( 0.000000000000000000, 1.000000000000000000, 0.000000000000000000 ) ) ;
#7450=VERTEX_POINT ( 'NONE', #14093 ) ;
#7472=CIRCLE ( 'NONE', #5986, 1.771449424009391427 ) ;
#7474=CARTESIAN_POINT ( 'NONE',  ( 109.7555300068681419, 1.750000000000000000, 36.44134644672088541 ) ) ;
#7516=LINE ( 'NONE', #3037, #2736 ) ;
#7572=CARTESIAN_POINT ( 'NONE',  ( 1.635615696801046015, 1.750000000000000000, -0.6802899045268993028 ) ) ;
#7647=DIRECTION ( 'NONE',  ( 0.000000000000000000, 0.000000000000000000, 1.000000000000000000 ) ) ;
#7656=ORIENTED_EDGE ( 'NONE', *, *, #14056, .F. ) ;
#7657=DIRECTION ( 'NONE',  ( 0.000000000000000000, 0.000000000000000000, -1.000000000000000000 ) ) ;
#7756=ORIENTED_EDGE ( 'NONE', *, *, #2031, .F. ) ;
#7758=DIRECTION ( 'NONE',  ( -0.000000000000000000, -1.000000000000000000, -0.000000000000000000 ) ) ;
#7764=AXIS2_PLACEMENT_3D ( 'NONE', #4998, #9863, #9941 ) ;
#7805=CARTESIAN_POINT ( 'NONE',  ( 33.75578156417349618, 0.000000000000000000, 39.47650855366864420 ) ) ;
#7847=ORIENTED_EDGE ( 'NONE', *, *, #13250, .T. ) ;
#7858=FACE_OUTER_BOUND ( 'NONE', #1560, .T. ) ;
#7863=DIRECTION ( 'NONE',  ( 0.02693067314564481438, -0.8090169943749466741, -0.5871679841888947093 ) ) ;
#7867=CARTESIAN_POINT ( 'NONE',  ( 4.030605408878806806, -2.051692149507289097E-14, 7.295648618995384638 ) ) ;
#7905=ADVANCED_FACE ( 'NONE', ( #4120 ), #13478, .F. ) ;
#7972=CARTESIAN_POINT ( 'NONE',  ( -2.357250054738958767, 2.100000000000253664, -0.4319429197694263367 ) ) ;
#7979=DIRECTION ( 'NONE',  ( 0.000000000000000000, 0.000000000000000000, 1.000000000000000000 ) ) ;
#8006=CARTESIAN_POINT ( 'NONE',  ( -5.609161682253958503, 1.749999999999405365, 27.59976306049381378 ) ) ;
#8042=DIRECTION ( 'NONE',  ( -0.000000000000000000, 1.000000000000000000, -0.000000000000000000 ) ) ;
#8045=CARTESIAN_POINT ( 'NONE',  ( -0.3675725891509502574, 0.000000000000000000, -0.3389548520155299949 ) ) ;
#8054=CARTESIAN_POINT ( 'NONE',  ( 38.58381714758451864, 1.749999999999999778, 41.14817863027235489 ) ) ;
#8066=CARTESIAN_POINT ( 'NONE',  ( 0.000000000000000000, 0.000000000000000000, 0.000000000000000000 ) ) ;
#8094=EDGE_CURVE ( 'NONE', #8895, #7450, #6072, .T. ) ;
#8098=DIRECTION ( 'NONE',  ( 0.000000000000000000, 0.000000000000000000, 1.000000000000000000 ) ) ;
#8114=CARTESIAN_POINT ( 'NONE',  ( 0.4616602863826355096, 0.000000000000000000, -0.1920150514337515824 ) ) ;
#8137=DIRECTION ( 'NONE',  ( -0.5425857474536051051, -0.8090169943749466741, 0.2260358588205426955 ) ) ;
#8145=CARTESIAN_POINT ( 'NONE',  ( -5.542419796536699472, 2.331468351712828340E-16, 11.20594165676177134 ) ) ;
#8166=VECTOR ( 'NONE', #10065, 1000.000000000000227 ) ;
#8175=PRODUCT_DEFINITION_SHAPE ( 'NONE', 'NONE',  #1046 ) ;
#8195=CARTESIAN_POINT ( 'NONE',  ( 0.9523100111875539842, 0.000000000000000000, 41.35525398876907133 ) ) ;
#8215=FACE_OUTER_BOUND ( 'NONE', #12791, .T. ) ;
#8223=CARTESIAN_POINT ( 'NONE',  ( -5.599503270685788792, 2.331468351713656644E-16, 20.51657426689472885 ) ) ;
#8281=CARTESIAN_POINT ( 'NONE',  ( 3.130150272509794274, 1.749999999999379829, 2.913007886993950191 ) ) ;
#8304=PRODUCT ( 'Blade_Predeterminado', 'Blade_Predeterminado', '', ( #3616 ) ) ;
#8323=ORIENTED_EDGE ( 'NONE', *, *, #10540, .T. ) ;
#8347=EDGE_LOOP ( 'NONE', ( #7656, #7104, #10321, #3546 ) ) ;
#8352=DIRECTION ( 'NONE',  ( 0.000000000000000000, 0.000000000000000000, -1.000000000000000000 ) ) ;
#8382=VECTOR ( 'NONE', #6797, 1000.000000000000000 ) ;
#8424=ORIENTED_EDGE ( 'NONE', *, *, #6940, .F. ) ;
#8437=EDGE_CURVE ( 'NONE', #10316, #8996, #7472, .T. ) ;
#8474=PLANE ( 'NONE',  #14123 ) ;
#8483=AXIS2_PLACEMENT_3D ( 'NONE', #9142, #7758, #7979 ) ;
#8487=CARTESIAN_POINT ( 'NONE',  ( 0.000000000000000000, 0.000000000000000000, -0.5000000000000018874 ) ) ;
#8512=CARTESIAN_POINT ( 'NONE',  ( 22.93326999583280923, 1.750000000002257083, 28.81042027259682214 ) ) ;
#8534=ADVANCED_FACE ( 'NONE', ( #9257 ), #4251, .F. ) ;
#8561=EDGE_CURVE ( 'NONE', #8996, #10252, #3148, .T. ) ;
#8657=CARTESIAN_POINT ( 'NONE',  ( 18.44985294524427388, 0.000000000000000000, 26.15777747556342803 ) ) ;
#8688=ORIENTED_EDGE ( 'NONE', *, *, #8437, .F. ) ;
#8735=VECTOR ( 'NONE', #5099, 1000.000000000000000 ) ;
#8737=CIRCLE ( 'NONE', #14677, 1.771449424009377438 ) ;
#8739=CARTESIAN_POINT ( 'NONE',  ( 19.54788354410667139, 2.100000000000000089, 25.09616337804641972 ) ) ;
#8788=EDGE_LOOP ( 'NONE', ( #7057, #39, #8688, #13871 ) ) ;
#8809=CARTESIAN_POINT ( 'NONE',  ( 30.32986759126112730, 1.750000000000000000, 39.54214087805579680 ) ) ;
#8858=DIRECTION ( 'NONE',  ( 0.000000000000000000, 1.000000000000000000, 0.000000000000000000 ) ) ;
#8862=CARTESIAN_POINT ( 'NONE',  ( 51.62524086895221842, 0.000000000000000000, 69.88209797381232136 ) ) ;
#8889=CARTESIAN_POINT ( 'NONE',  ( 38.72419741971091867, 2.100000000000000089, 40.93614862128714549 ) ) ;
#8891=DIRECTION ( 'NONE',  ( 0.000000000000000000, 0.000000000000000000, 1.000000000000000000 ) ) ;
#8895=VERTEX_POINT ( 'NONE', #8862 ) ;
#8951=DIRECTION ( 'NONE',  ( -0.000000000000000000, 1.000000000000000000, -0.000000000000000000 ) ) ;
#8954=EDGE_CURVE ( 'NONE', #2235, #10316, #3842, .T. ) ;
#8961=DIRECTION ( 'NONE',  ( 0.000000000000000000, 0.000000000000000000, 1.000000000000000000 ) ) ;
#8963=CARTESIAN_POINT ( 'NONE',  ( 3.358120751865298903, 2.099999999996547295, 2.798954194608255897 ) ) ;
#8996=VERTEX_POINT ( 'NONE', #3067 ) ;
#9091=DIRECTION ( 'NONE',  ( 0.000000000000000000, 0.000000000000000000, 1.000000000000000000 ) ) ;
#9138=FACE_OUTER_BOUND ( 'NONE', #11548, .T. ) ;
#9142=CARTESIAN_POINT ( 'NONE',  ( 30.32986759126112730, 0.7500000000000000000, 43.04214087805580391 ) ) ;
#9221=VERTEX_POINT ( 'NONE', #9704 ) ;
#9225=FACE_OUTER_BOUND ( 'NONE', #6218, .T. ) ;
#9226=DIRECTION ( 'NONE',  ( 0.000000000000000000, 0.000000000000000000, 1.000000000000000000 ) ) ;
#9257=FACE_OUTER_BOUND ( 'NONE', #4262, .T. ) ;
#9286=CARTESIAN_POINT ( 'NONE',  ( -4.841311305102414586, 2.099999999999999645, 31.26088239576554173 ) ) ;
#9305=DIRECTION ( 'NONE',  ( -0.000000000000000000, -1.000000000000000000, -0.000000000000000000 ) ) ;
#9325=EDGE_CURVE ( 'NONE', #11802, #8895, #85, .T. ) ;
#9326=FACE_OUTER_BOUND ( 'NONE', #13694, .T. ) ;
#9330=DIRECTION ( 'NONE',  ( 0.000000000000000000, 0.000000000000000000, 1.000000000000000000 ) ) ;
#9357=CARTESIAN_POINT ( 'NONE',  ( -5.599503270685788792, 0.000000000000000000, 20.51657426689472885 ) ) ;
#9359=CARTESIAN_POINT ( 'NONE',  ( 30.32986759126112730, 0.000000000000000000, 41.04214087805579680 ) ) ;
#9366=DIRECTION ( 'NONE',  ( 0.000000000000000000, 1.000000000000000000, 0.000000000000000000 ) ) ;
#9419=AXIS2_PLACEMENT_3D ( 'NONE', #15272, #9226, #12943 ) ;
#9440=CARTESIAN_POINT ( 'NONE',  ( 52.73038795364751508, 1.750000000000000000, 69.25342193720584305 ) ) ;
#9448=DIRECTION ( 'NONE',  ( 0.000000000000000000, 0.000000000000000000, 1.000000000000000000 ) ) ;
#9462=AXIS2_PLACEMENT_3D ( 'NONE', #12682, #1010, #3328 ) ;
#9611=LINE ( 'NONE', #12080, #12111 ) ;
#9651=AXIS2_PLACEMENT_3D ( 'NONE', #1667, #14444, #10861 ) ;
#9671=B_SPLINE_SURFACE_WITH_KNOTS ( 'NONE', 1, 3, ( 
 ( #10447, #7972, #14084, #2403, #4579, #11601, #10672, #11531, #1097, #15257, #9286, #7033, #14011, #945, #4727, #3337, #10370, #5870, #12846, #2259 ),
 ( #8045, #6965, #5802, #10524, #5649, #1023, #4648, #15108, #9357, #5728, #12773, #2180, #8195, #12926, #14165, #11747, #3568, #12999, #7101, #11820 ) ),
 .UNSPECIFIED., .F., .F., .F.,
 ( 2, 2 ),
 ( 4, 2, 2, 2, 2, 2, 2, 2, 2, 4 ),
 ( 0.000000000000000000, 1.000000000000000000 ),
 ( 0.1367849146739316402, 0.2678915559620899112, 0.3989981972502481544, 0.6612114798265646964, 0.9234247624028811829, 1.185638044979197669, 1.447851327555514267, 1.710064610131830642, 1.972277892708147018, 2.234491175284463615 ),
 .UNSPECIFIED. ) ;
#9704=CARTESIAN_POINT ( 'NONE',  ( 0.000000000000000000, 1.750000000000000000, -1.771449424009386986 ) ) ;
#9714=EDGE_CURVE ( 'NONE', #7450, #1764, #15163, .T. ) ;
#9725=DIRECTION ( 'NONE',  ( 0.000000000000000000, 1.000000000000000000, 0.000000000000000000 ) ) ;
#9730=AXIS2_PLACEMENT_3D ( 'NONE', #9813, #11048, #9091 ) ;
#9785=EDGE_CURVE ( 'NONE', #10699, #922, #11763, .T. ) ;
#9796=CARTESIAN_POINT ( 'NONE',  ( -2.923188566258836385, 1.750000000000027756, 0.7596801491339106871 ) ) ;
#9813=CARTESIAN_POINT ( 'NONE',  ( 30.32986759126112730, 0.7500000000000000000, 43.04214087805580391 ) ) ;
#9827=ORIENTED_EDGE ( 'NONE', *, *, #7409, .F. ) ;
#9863=DIRECTION ( 'NONE',  ( 0.000000000000000000, 1.000000000000000000, 0.000000000000000000 ) ) ;
#9887=VECTOR ( 'NONE', #4729, 1000.000000000000114 ) ;
#9941=DIRECTION ( 'NONE',  ( 0.000000000000000000, 0.000000000000000000, -1.000000000000000000 ) ) ;
#9957=CIRCLE ( 'NONE', #6998, 0.5000000000000018874 ) ;
#9959=AXIS2_PLACEMENT_3D ( 'NONE', #12750, #11656, #8098 ) ;
#10003=LINE ( 'NONE', #6597, #14323 ) ;
#10014=EDGE_CURVE ( 'NONE', #6135, #13423, #9957, .T. ) ;
#10031=CARTESIAN_POINT ( 'NONE',  ( 30.32986759126112730, 0.7500000000000000000, 46.54214087805580391 ) ) ;
#10046=CARTESIAN_POINT ( 'NONE',  ( 8.994679575448120801, -2.051692149507289097E-14, 14.93252568749840847 ) ) ;
#10065=DIRECTION ( 'NONE',  ( 0.000000000000000000, 0.8090169943749465631, 0.5877852522924742473 ) ) ;
#10119=CARTESIAN_POINT ( 'NONE',  ( 1.990297875723435084, -2.051692149503915928E-14, 3.483276348926839461 ) ) ;
#10160=AXIS2_PLACEMENT_3D ( 'NONE', #10221, #5643, #11295 ) ;
#10221=CARTESIAN_POINT ( 'NONE',  ( 51.19063959271458231, 0.000000000000000000, 70.12932606827693860 ) ) ;
#10248=ORIENTED_EDGE ( 'NONE', *, *, #6779, .F. ) ;
#10252=VERTEX_POINT ( 'NONE', #1640 ) ;
#10269=CARTESIAN_POINT ( 'NONE',  ( 29.71057115341583454, -2.051692149507289097E-14, 36.39324188472026123 ) ) ;
#10271=CARTESIAN_POINT ( 'NONE',  ( 26.04203104729492679, 0.000000000000000000, 69.41411580402544246 ) ) ;
#10273=DIRECTION ( 'NONE',  ( 0.000000000000000000, 1.000000000000000000, 0.000000000000000000 ) ) ;
#10274=DIRECTION ( 'NONE',  ( 0.9989498407774403121, 0.000000000000000000, 0.04581719776161458091 ) ) ;
#10288=LINE ( 'NONE', #3107, #8166 ) ;
#10291=DIRECTION ( 'NONE',  ( 0.000000000000000000, 0.000000000000000000, -1.000000000000000000 ) ) ;
#10316=VERTEX_POINT ( 'NONE', #11145 ) ;
#10318=DIRECTION ( 'NONE',  ( 0.000000000000000000, 0.000000000000000000, 1.000000000000000000 ) ) ;
#10321=ORIENTED_EDGE ( 'NONE', *, *, #1112, .F. ) ;
#10351=ORIENTED_EDGE ( 'NONE', *, *, #13747, .F. ) ;
#10367=DIRECTION ( 'NONE',  ( 0.000000000000000000, 0.000000000000000000, 1.000000000000000000 ) ) ;
#10370=CARTESIAN_POINT ( 'NONE',  ( 13.59058908281841482, 2.099999999999187850, 61.49439185523788609 ) ) ;
#10394=CARTESIAN_POINT ( 'NONE',  ( 38.25296960060453699, 0.000000000000000000, 42.65758570601131794 ) ) ;
#10399=CIRCLE ( 'NONE', #5698, 1.771449424009377438 ) ;
#10403=CARTESIAN_POINT ( 'NONE',  ( 51.19063959271458231, 1.750000000000000000, 70.12932606827693860 ) ) ;
#10408=CARTESIAN_POINT ( 'NONE',  ( 22.39039888797916333, 1.750000000000027756, 68.66652033670405331 ) ) ;
#10435=CARTESIAN_POINT ( 'NONE',  ( 51.62524086895221842, 0.000000000000000000, 69.88209797381232136 ) ) ;
#10443=VECTOR ( 'NONE', #7863, 1000.000000000000000 ) ;
#10447=CARTESIAN_POINT ( 'NONE',  ( -1.489212485369225458, 2.100000000000000089, -1.373268335280311891 ) ) ;
#10479=CARTESIAN_POINT ( 'NONE',  ( 37.88191578704504536, 0.000000000000000000, 42.20832867525968624 ) ) ;
#10484=CONICAL_SURFACE ( 'NONE', #1602, 0.5000000000000018874, 0.6283185307179600665 ) ;
#10524=CARTESIAN_POINT ( 'NONE',  ( -3.125658737029940681, 0.000000000000000000, 3.587914672538146554 ) ) ;
#10526=LINE ( 'NONE', #15259, #9887 ) ;
#10537=CARTESIAN_POINT ( 'NONE',  ( 42.09231163430414568, 0.000000000000000000, 51.87369981213807080 ) ) ;
#10540=EDGE_CURVE ( 'NONE', #11406, #10699, #11207, .T. ) ;
#10573=ORIENTED_EDGE ( 'NONE', *, *, #7100, .F. ) ;
#10618=CARTESIAN_POINT ( 'NONE',  ( -3.384109865120556560, 2.331468351712828340E-16, 30.80069534665370767 ) ) ;
#10666=PRODUCT_DEFINITION_FORMATION_WITH_SPECIFIED_SOURCE ( 'ANY', '', #8304, .NOT_KNOWN. ) ;
#10672=CARTESIAN_POINT ( 'NONE',  ( -7.059949148491517334, 2.099999999999999645, 11.00002213459155875 ) ) ;
#10693=ORIENTED_EDGE ( 'NONE', *, *, #13683, .F. ) ;
#10699=VERTEX_POINT ( 'NONE', #1227 ) ;
#10786=CLOSED_SHELL ( 'NONE', ( #8534, #14058, #11945, #11875, #7905, #4117, #13115, #918, #11604, #12335, #3014, #11269, #2429, #14748, #5906, #5126, #1924 ) ) ;
#10836=EDGE_CURVE ( 'NONE', #13395, #14298, #11412, .T. ) ;
#10861=DIRECTION ( 'NONE',  ( 0.000000000000000000, 0.000000000000000000, 1.000000000000000000 ) ) ;
#10884=EDGE_CURVE ( 'NONE', #14114, #3665, #14937, .T. ) ;
#10891=SHAPE_REPRESENTATION ( 'Blade_Predeterminado', ( #9419 ), #12893 ) ;
#11048=DIRECTION ( 'NONE',  ( 0.000000000000000000, 1.000000000000000000, 0.000000000000000000 ) ) ;
#11079=DIRECTION ( 'NONE',  ( -0.5427142158096631697, -0.8090169943749466741, 0.2257272309018785728 ) ) ;
#11095=VERTEX_POINT ( 'NONE', #11108 ) ;
#11108=CARTESIAN_POINT ( 'NONE',  ( 51.19063959271458231, 1.750000000000000000, 71.90077549228632847 ) ) ;
#11119=EDGE_CURVE ( 'NONE', #14114, #12741, #5090, .T. ) ;
#11133=CARTESIAN_POINT ( 'NONE',  ( 34.65560150440948206, 2.100000000001073008, 38.24242331140461459 ) ) ;
#11134=CONICAL_SURFACE ( 'NONE', #10160, 0.4999999999999865663, 0.6283185307179600665 ) ;
#11137=UNCERTAINTY_MEASURE_WITH_UNIT (LENGTH_MEASURE( 1.000000000000000082E-05 ), #1419, 'distance_accuracy_value', 'NONE');
#11145=CARTESIAN_POINT ( 'NONE',  ( 25.37742002255717466, 1.750000000000000000, 70.49803269364883818 ) ) ;
#11181=AXIS2_PLACEMENT_3D ( 'NONE', #13983, #8951, #13681 ) ;
#11207=CIRCLE ( 'NONE', #2328, 2.271449424009384987 ) ;
#11212=CARTESIAN_POINT ( 'NONE',  ( 5.354258359986379112, 2.100000000000000089, 6.532454833391891036 ) ) ;
#11257=CARTESIAN_POINT ( 'NONE',  ( -4.598444398438791936, 1.750000000000027311, 31.18418455424690805 ) ) ;
#11269=ADVANCED_FACE ( 'NONE', ( #7858 ), #13674, .T. ) ;
#11276=CIRCLE ( 'NONE', #7316, 3.500000000000003109 ) ;
#11281=CARTESIAN_POINT ( 'NONE',  ( 30.32986759126112730, 0.7500000000000000000, 43.04214087805580391 ) ) ;
#11288=EDGE_LOOP ( 'NONE', ( #11535, #6832, #1956, #2170 ) ) ;
#11289=DIRECTION ( 'NONE',  ( -0.000000000000000000, -1.000000000000000000, -0.000000000000000000 ) ) ;
#11295=DIRECTION ( 'NONE',  ( 0.000000000000000000, 0.000000000000000000, 1.000000000000000000 ) ) ;
#11333=CARTESIAN_POINT ( 'NONE',  ( 30.32986759126112730, 0.7500000000000000000, 39.54214087805579680 ) ) ;
#11406=VERTEX_POINT ( 'NONE', #4685 ) ;
#11411=CARTESIAN_POINT ( 'NONE',  ( 6.079769598696780797, 1.750000000000736966, 52.20213348949025089 ) ) ;
#11412=LINE ( 'NONE', #2863, #8735 ) ;
#11433=DIRECTION ( 'NONE',  ( 0.000000000000000000, 1.000000000000000000, 0.000000000000000000 ) ) ;
#11442=CARTESIAN_POINT ( 'NONE',  ( 42.09231163430414568, 1.632027846204027168E-15, 51.87369981213807080 ) ) ;
#11462=ORIENTED_EDGE ( 'NONE', *, *, #2812, .T. ) ;
#11499=ORIENTED_EDGE ( 'NONE', *, *, #8561, .T. ) ;
#11515=DIRECTION ( 'NONE',  ( 0.000000000000000000, 1.000000000000000000, 0.000000000000000000 ) ) ;
#11524=FACE_OUTER_BOUND ( 'NONE', #11567, .T. ) ;
#11531=CARTESIAN_POINT ( 'NONE',  ( -7.366917200155316259, 2.099999999999999645, 17.31320944260497541 ) ) ;
#11535=ORIENTED_EDGE ( 'NONE', *, *, #7100, .T. ) ;
#11548=EDGE_LOOP ( 'NONE', ( #841, #8424, #3802, #6909 ) ) ;
#11564=DIRECTION ( 'NONE',  ( -0.03706689162378395269, -0.5877852522924743583, 0.8081673977170961143 ) ) ;
#11567=EDGE_LOOP ( 'NONE', ( #11880, #13950, #10693, #6223 ) ) ;
#11580=ORIENTED_EDGE ( 'NONE', *, *, #8954, .T. ) ;
#11594=VECTOR ( 'NONE', #8137, 1000.000000000000000 ) ;
#11601=CARTESIAN_POINT ( 'NONE',  ( -6.505077406322743450, 2.100000000000000089, 8.060717365551118618 ) ) ;
#11604=ADVANCED_FACE ( 'NONE', ( #6147 ), #4792, .T. ) ;
#11618=DIRECTION ( 'NONE',  ( 0.000000000000000000, -0.000000000000000000, 1.000000000000000000 ) ) ;
#11630=ORIENTED_EDGE ( 'NONE', *, *, #13747, .T. ) ;
#11638=B_SPLINE_SURFACE_WITH_KNOTS ( 'NONE', 1, 3, ( 
 ( #4439, #3421, #2123, #1115 ),
 ( #13954, #958, #10537, #2274 ) ),
 .UNSPECIFIED., .F., .F., .F.,
 ( 2, 2 ),
 ( 4, 4 ),
 ( 0.000000000000000000, 1.000000000000000000 ),
 ( 4.709001436419550934, 4.943672903615365932 ),
 .UNSPECIFIED. ) ;
#11656=DIRECTION ( 'NONE',  ( 0.000000000000000000, 1.000000000000000000, 0.000000000000000000 ) ) ;
#11680=FACE_OUTER_BOUND ( 'NONE', #11288, .T. ) ;
#11719=ORIENTED_EDGE ( 'NONE', *, *, #1110, .F. ) ;
#11747=CARTESIAN_POINT ( 'NONE',  ( 12.01748009419283925, 0.000000000000000000, 57.58516622398010298 ) ) ;
#11763=B_SPLINE_CURVE_WITH_KNOTS ( 'NONE', 3,
 ( #8054, #12782, #886, #8512, #12148, #3809, #1565, #2576, #8281, #1337 ),
 .UNSPECIFIED., .F., .F.,
 ( 4, 2, 2, 2, 4 ),
 ( 0.000000000000000000, 0.01417170859615501759, 0.02834341719231003517, 0.04251512578846505103, 0.05668683438462007035 ),
 .UNSPECIFIED. ) ;
#11772=LINE ( 'NONE', #2587, #2755 ) ;
#11776=CARTESIAN_POINT ( 'NONE',  ( 0.9523100111875538731, 2.331468351713773987E-16, 41.35525398876907133 ) ) ;
#11802=VERTEX_POINT ( 'NONE', #2506 ) ;
#11820=CARTESIAN_POINT ( 'NONE',  ( 26.04203104729493390, 0.000000000000000000, 69.41411580402545667 ) ) ;
#11825=ORIENTED_EDGE ( 'NONE', *, *, #4891, .F. ) ;
#11835=CARTESIAN_POINT ( 'NONE',  ( 109.7555300068681419, 0.000000000000000000, 36.44134644672088541 ) ) ;
#11847=DIRECTION ( 'NONE',  ( -0.3244857880293323671, -0.8090169943749464521, 0.4901025159897783312 ) ) ;
#11875=ADVANCED_FACE ( 'NONE', ( #4522 ), #5669, .F. ) ;
#11880=ORIENTED_EDGE ( 'NONE', *, *, #6545, .T. ) ;
#11887=CARTESIAN_POINT ( 'NONE',  ( 37.32986759126112730, 1.750000000000000000, 43.04214087805580391 ) ) ;
#11926=ORIENTED_EDGE ( 'NONE', *, *, #3195, .T. ) ;
#11945=ADVANCED_FACE ( 'NONE', ( #8215 ), #10484, .T. ) ;
#11977=DIRECTION ( 'NONE',  ( -0.000000000000000000, 1.000000000000000000, -0.000000000000000000 ) ) ;
#12060=ORIENTED_EDGE ( 'NONE', *, *, #7409, .T. ) ;
#12080=CARTESIAN_POINT ( 'NONE',  ( 30.32986759126112730, 1.750000000000000000, 45.04214087805580391 ) ) ;
#12081=ORIENTED_EDGE ( 'NONE', *, *, #8437, .T. ) ;
#12111=VECTOR ( 'NONE', #3743, 1000.000000000000000 ) ;
#12148=CARTESIAN_POINT ( 'NONE',  ( 19.36487844429745309, 1.750000000002257083, 25.27309906096478187 ) ) ;
#12167=EDGE_LOOP ( 'NONE', ( #2373, #10248 ) ) ;
#12186=CARTESIAN_POINT ( 'NONE',  ( -6.256102584674404277, 1.750000000000027756, 8.120257307136867553 ) ) ;
#12188=CIRCLE ( 'NONE', #9959, 0.4999999999999865663 ) ;
#12198=EDGE_LOOP ( 'NONE', ( #15211, #615, #963, #14847 ) ) ;
#12217=VECTOR ( 'NONE', #10274, 999.9999999999998863 ) ;
#12218=CARTESIAN_POINT ( 'NONE',  ( 4.030605408878820128, 0.000000000000000000, 7.295648618995377532 ) ) ;
#12235=DIRECTION ( 'NONE',  ( 0.000000000000000000, 0.8090169943749465631, -0.5877852522924742473 ) ) ;
#12242=ORIENTED_EDGE ( 'NONE', *, *, #2538, .T. ) ;
#12293=CARTESIAN_POINT ( 'NONE',  ( -1.302272502657875197, 1.750000000000000000, -1.200882754745186798 ) ) ;
#12335=ADVANCED_FACE ( 'NONE', ( #11680 ), #9671, .T. ) ;
#12361=CARTESIAN_POINT ( 'NONE',  ( 33.75578156417348907, -2.051692149508337651E-14, 39.47650855366865841 ) ) ;
#12388=DIRECTION ( 'NONE',  ( 0.000000000000000000, 1.000000000000000000, 0.000000000000000000 ) ) ;
#12413=CARTESIAN_POINT ( 'NONE',  ( -6.865783330443320231, 1.750000000000649258, 20.65929969372286479 ) ) ;
#12445=CARTESIAN_POINT ( 'NONE',  ( 13.10812892772005966, 2.100000000000000089, 17.79937169134660024 ) ) ;
#12454=MANIFOLD_SOLID_BREP ( 'Cortar-Extruir2', #10786 ) ;
#12455=CARTESIAN_POINT ( 'NONE',  ( 30.32986759126112730, 1.750000000000000000, 43.04214087805580391 ) ) ;
#12577=DIRECTION ( 'NONE',  ( -0.000000000000000000, 1.000000000000000000, -0.000000000000000000 ) ) ;
#12592=PLANE ( 'NONE',  #6435 ) ;
#12594=EDGE_LOOP ( 'NONE', ( #7189, #3051, #783, #11719, #14266, #10573, #11825, #13262, #12648, #15139 ) ) ;
#12643=ORIENTED_EDGE ( 'NONE', *, *, #555, .T. ) ;
#12648=ORIENTED_EDGE ( 'NONE', *, *, #14349, .F. ) ;
#12672=ORIENTED_EDGE ( 'NONE', *, *, #6168, .F. ) ;
#12682=CARTESIAN_POINT ( 'NONE',  ( 51.19063959271458231, 0.000000000000000000, 70.12932606827693860 ) ) ;
#12684=VECTOR ( 'NONE', #14533, 1000.000000000000000 ) ;
#12690=LINE ( 'NONE', #14162, #3490 ) ;
#12698=DIRECTION ( 'NONE',  ( 0.000000000000000000, 0.000000000000000000, -1.000000000000000000 ) ) ;
#12699=ORIENTED_EDGE ( 'NONE', *, *, #11119, .T. ) ;
#12741=VERTEX_POINT ( 'NONE', #13336 ) ;
#12743=CARTESIAN_POINT ( 'NONE',  ( 26.30339064689345463, 1.750000000000000000, 68.98786334397659914 ) ) ;
#12750=CARTESIAN_POINT ( 'NONE',  ( 51.19063959271458231, 0.000000000000000000, 70.12932606827693860 ) ) ;
#12771=VECTOR ( 'NONE', #5294, 1000.000000000000000 ) ;
#12773=CARTESIAN_POINT ( 'NONE',  ( -3.384109865120556560, 0.000000000000000000, 30.80069534665370767 ) ) ;
#12782=CARTESIAN_POINT ( 'NONE',  ( 34.50563151437111742, 1.750000000003151257, 38.44810418511396222 ) ) ;
#12791=EDGE_LOOP ( 'NONE', ( #3467, #4603, #1502, #11462 ) ) ;
#12798=CARTESIAN_POINT ( 'NONE',  ( -1.160594694320683518, 2.331468351713110358E-16, 0.5210215923759189405 ) ) ;
#12801=ORIENTED_EDGE ( 'NONE', *, *, #10884, .T. ) ;
#12846=CARTESIAN_POINT ( 'NONE',  ( 22.24275793208308016, 2.100000000000000089, 68.87427881220452264 ) ) ;
#12893=( GEOMETRIC_REPRESENTATION_CONTEXT ( 3 ) GLOBAL_UNCERTAINTY_ASSIGNED_CONTEXT ( ( #11137 ) ) GLOBAL_UNIT_ASSIGNED_CONTEXT ( ( #1419, #5967, #7197 ) ) REPRESENTATION_CONTEXT ( 'NONE', 'WORKASPACE' ) );
#12926=CARTESIAN_POINT ( 'NONE',  ( 4.869735923794943133, 0.000000000000000000, 48.16793894843318924 ) ) ;
#12939=B_SPLINE_CURVE_WITH_KNOTS ( 'NONE', 3,
 ( #9440, #2405, #15110, #14168 ),
 .UNSPECIFIED., .F., .F.,
 ( 4, 4 ),
 ( 0.000000000000000000, 0.03019882497682960937 ),
 .UNSPECIFIED. ) ;
#12943=DIRECTION ( 'NONE',  ( 1.000000000000000000, 0.000000000000000000, 0.000000000000000000 ) ) ;
#12954=CARTESIAN_POINT ( 'NONE',  ( -4.373225680752619304, 2.331468351711999543E-16, 27.28944397070847927 ) ) ;
#12999=CARTESIAN_POINT ( 'NONE',  ( 20.23335552821398409, 0.000000000000000000, 65.44177069175029260 ) ) ;
#13070=DIRECTION ( 'NONE',  ( -0.000000000000000000, -1.000000000000000000, -0.000000000000000000 ) ) ;
#13106=AXIS2_PLACEMENT_3D ( 'NONE', #11835, #1114, #11618 ) ;
#13115=ADVANCED_FACE ( 'NONE', ( #9138 ), #1997, .T. ) ;
#13117=ORIENTED_EDGE ( 'NONE', *, *, #10836, .F. ) ;
#13187=ORIENTED_EDGE ( 'NONE', *, *, #4618, .T. ) ;
#13250=EDGE_CURVE ( 'NONE', #8996, #13395, #10526, .T. ) ;
#13258=VERTEX_POINT ( 'NONE', #9359 ) ;
#13262=ORIENTED_EDGE ( 'NONE', *, *, #10014, .F. ) ;
#13276=EDGE_CURVE ( 'NONE', #5602, #11406, #12939, .T. ) ;
#13336=CARTESIAN_POINT ( 'NONE',  ( 30.32986759126112730, 1.750000000000000000, 46.54214087805580391 ) ) ;
#13360=CARTESIAN_POINT ( 'NONE',  ( -4.834347064118100334, 1.750000000000027756, 4.227958732727228330 ) ) ;
#13395=VERTEX_POINT ( 'NONE', #5111 ) ;
#13423=VERTEX_POINT ( 'NONE', #8487 ) ;
#13470=CARTESIAN_POINT ( 'NONE',  ( 11.91826453496365623, 0.000000000000000000, 18.75693026131819963 ) ) ;
#13478=CYLINDRICAL_SURFACE ( 'NONE', #13904, 2.000000000000001776 ) ;
#13674=PLANE ( 'NONE',  #4061 ) ;
#13681=DIRECTION ( 'NONE',  ( 0.000000000000000000, 0.000000000000000000, 1.000000000000000000 ) ) ;
#13683=EDGE_CURVE ( 'NONE', #13395, #11095, #10399, .T. ) ;
#13694=EDGE_LOOP ( 'NONE', ( #12801, #1249 ) ) ;
#13747=EDGE_CURVE ( 'NONE', #9221, #2235, #6203, .T. ) ;
#13748=DIRECTION ( 'NONE',  ( 0.000000000000000000, -0.8087231630780308267, -0.5881894639493849830 ) ) ;
#13787=FACE_OUTER_BOUND ( 'NONE', #8788, .T. ) ;
#13830=CARTESIAN_POINT ( 'NONE',  ( 22.05734493763781146, -2.051692149507289097E-14, 29.73364058993714565 ) ) ;
#13863=DIRECTION ( 'NONE',  ( 0.000000000000000000, 0.000000000000000000, 1.000000000000000000 ) ) ;
#13871=ORIENTED_EDGE ( 'NONE', *, *, #164, .T. ) ;
#13872=AXIS2_PLACEMENT_3D ( 'NONE', #14752, #5304, #5230 ) ;
#13904=AXIS2_PLACEMENT_3D ( 'NONE', #12455, #11289, #7657 ) ;
#13930=CARTESIAN_POINT ( 'NONE',  ( -0.3675725891509502574, 0.000000000000000000, -0.3389548520155299949 ) ) ;
#13950=ORIENTED_EDGE ( 'NONE', *, *, #14056, .T. ) ;
#13954=CARTESIAN_POINT ( 'NONE',  ( 51.62524086895222553, 0.000000000000000000, 69.88209797381236399 ) ) ;
#13983=CARTESIAN_POINT ( 'NONE',  ( 30.32986759126112730, 0.7500000000000000000, 43.04214087805580391 ) ) ;
#14010=DIRECTION ( 'NONE',  ( 0.000000000000000000, 1.000000000000000000, 0.000000000000000000 ) ) ;
#14011=CARTESIAN_POINT ( 'NONE',  ( -0.4094286939087771193, 2.100000000000851408, 42.04785295243777199 ) ) ;
#14029=DIRECTION ( 'NONE',  ( 0.000000000000000000, 1.000000000000000000, 0.000000000000000000 ) ) ;
#14037=CARTESIAN_POINT ( 'NONE',  ( -3.665378489062163236, 2.331468351712828833E-16, 4.733462801983808532 ) ) ;
#14050=CARTESIAN_POINT ( 'NONE',  ( 30.32986759126112730, 0.7500000000000000000, 43.04214087805580391 ) ) ;
#14056=EDGE_CURVE ( 'NONE', #11802, #11095, #10288, .T. ) ;
#14058=ADVANCED_FACE ( 'NONE', ( #11524 ), #11134, .T. ) ;
#14084=CARTESIAN_POINT ( 'NONE',  ( -3.133172996766207419, 2.100000000000000089, 0.6152778258340406703 ) ) ;
#14093=CARTESIAN_POINT ( 'NONE',  ( 38.25296960060453699, 0.000000000000000000, 42.65758570601131794 ) ) ;
#14114=VERTEX_POINT ( 'NONE', #15025 ) ;
#14123=AXIS2_PLACEMENT_3D ( 'NONE', #7474, #9725, #453 ) ;
#14162=CARTESIAN_POINT ( 'NONE',  ( 30.32986759126112730, 0.7500000000000000000, 39.54214087805579680 ) ) ;
#14165=CARTESIAN_POINT ( 'NONE',  ( 7.113306724408225534, 0.000000000000000000, 51.45871142768356066 ) ) ;
#14168=CARTESIAN_POINT ( 'NONE',  ( 39.42664711868611960, 1.750000000000000000, 42.16864325401552804 ) ) ;
#14191=VERTEX_POINT ( 'NONE', #1162 ) ;
#14247=DIRECTION ( 'NONE',  ( -0.000000000000000000, 1.000000000000000000, -0.000000000000000000 ) ) ;
#14266=ORIENTED_EDGE ( 'NONE', *, *, #1240, .F. ) ;
#14298=VERTEX_POINT ( 'NONE', #14305 ) ;
#14305=CARTESIAN_POINT ( 'NONE',  ( 51.16773099383375012, 0.000000000000000000, 70.62880098866567380 ) ) ;
#14323=VECTOR ( 'NONE', #11079, 1000.000000000000000 ) ;
#14349=EDGE_CURVE ( 'NONE', #1764, #6135, #3126, .T. ) ;
#14354=AXIS2_PLACEMENT_3D ( 'NONE', #1862, #11433, #8961 ) ;
#14444=DIRECTION ( 'NONE',  ( 0.000000000000000000, 1.000000000000000000, 0.000000000000000000 ) ) ;
#14491=CARTESIAN_POINT ( 'NONE',  ( 0.000000000000000000, 0.000000000000000000, 0.000000000000000000 ) ) ;
#14503=VERTEX_POINT ( 'NONE', #8809 ) ;
#14522=ORIENTED_EDGE ( 'NONE', *, *, #2595, .F. ) ;
#14533=DIRECTION ( 'NONE',  ( -0.000000000000000000, 1.000000000000000000, -0.000000000000000000 ) ) ;
#14610=FACE_BOUND ( 'NONE', #2513, .T. ) ;
#14616=CARTESIAN_POINT ( 'NONE',  ( 37.88191578704505957, 0.000000000000000000, 42.20832867525968624 ) ) ;
#14677=AXIS2_PLACEMENT_3D ( 'NONE', #10403, #8858, #10318 ) ;
#14708=CARTESIAN_POINT ( 'NONE',  ( 37.88191578704505957, 0.000000000000000000, 42.20832867525968624 ) ) ;
#14748=ADVANCED_FACE ( 'NONE', ( #14610, #4921 ), #8474, .T. ) ;
#14752=CARTESIAN_POINT ( 'NONE',  ( 30.32986759126112730, 1.750000000000000000, 43.04214087805580391 ) ) ;
#14812=ORIENTED_EDGE ( 'NONE', *, *, #4515, .F. ) ;
#14847=ORIENTED_EDGE ( 'NONE', *, *, #6940, .T. ) ;
#14860=CARTESIAN_POINT ( 'NONE',  ( 0.4616602863826355096, 0.000000000000000000, -0.1920150514337515824 ) ) ;
#14909=DIRECTION ( 'NONE',  ( 0.000000000000000000, -1.000000000000000000, 0.000000000000000000 ) ) ;
#14923=FACE_OUTER_BOUND ( 'NONE', #5935, .T. ) ;
#14934=ORIENTED_EDGE ( 'NONE', *, *, #6779, .T. ) ;
#14937=CIRCLE ( 'NONE', #9730, 3.500000000000003109 ) ;
#14940=DIRECTION ( 'NONE',  ( 0.000000000000000000, 0.000000000000000000, -1.000000000000000000 ) ) ;
#14949=AXIS2_PLACEMENT_3D ( 'NONE', #15275, #9305, #2195 ) ;
#14985=CARTESIAN_POINT ( 'NONE',  ( 11.06582261942825518, 1.749999999999318767, 58.43087504082885175 ) ) ;
#14995=DIRECTION ( 'NONE',  ( 0.000000000000000000, 1.000000000000000000, 0.000000000000000000 ) ) ;
#15011=CARTESIAN_POINT ( 'NONE',  ( 51.19063959271458231, 0.000000000000000000, 70.12932606827693860 ) ) ;
#15022=LINE ( 'NONE', #13930, #5691 ) ;
#15025=CARTESIAN_POINT ( 'NONE',  ( 30.32986759126112730, 0.7500000000000000000, 46.54214087805580391 ) ) ;
#15030=CARTESIAN_POINT ( 'NONE',  ( 30.32986759126112730, 1.750000000000000000, 43.04214087805580391 ) ) ;
#15035=ORIENTED_EDGE ( 'NONE', *, *, #9785, .T. ) ;
#15040=CARTESIAN_POINT ( 'NONE',  ( 37.32986759126112730, 0.000000000000000000, 43.04214087805580391 ) ) ;
#15041=ORIENTED_EDGE ( 'NONE', *, *, #6168, .T. ) ;
#15060=ORIENTED_EDGE ( 'NONE', *, *, #13276, .T. ) ;
#15061=CARTESIAN_POINT ( 'NONE',  ( -0.1824722430594065969, 1.750000000000737410, 41.93241979182633372 ) ) ;
#15108=CARTESIAN_POINT ( 'NONE',  ( -5.836568743579779728, 0.000000000000000000, 17.25548782215969368 ) ) ;
#15110=CARTESIAN_POINT ( 'NONE',  ( 43.24549764042590994, 1.750000000004062306, 51.33556869416222668 ) ) ;
#15139=ORIENTED_EDGE ( 'NONE', *, *, #9714, .F. ) ;
#15140=CARTESIAN_POINT ( 'NONE',  ( 19.43417530611593591, 1.750000000000704325, 66.43326964946760427 ) ) ;
#15163=CIRCLE ( 'NONE', #2065, 1.000000000000000888 ) ;
#15196=EDGE_CURVE ( 'NONE', #14503, #12741, #3744, .T. ) ;
#15211=ORIENTED_EDGE ( 'NONE', *, *, #14349, .T. ) ;
#15257=CARTESIAN_POINT ( 'NONE',  ( -5.856348882554203605, 2.099999999999253131, 27.66182687845087429 ) ) ;
#15259=CARTESIAN_POINT ( 'NONE',  ( 26.22222779830891781, 1.749999999999999778, 70.75745246403606359 ) ) ;
#15260=CARTESIAN_POINT ( 'NONE',  ( 30.32986759126112730, 0.7500000000000000000, 43.04214087805580391 ) ) ;
#15272=CARTESIAN_POINT ( 'NONE',  ( 0.000000000000000000, 0.000000000000000000, 0.000000000000000000 ) ) ;
#15275=CARTESIAN_POINT ( 'NONE',  ( 30.32986759126112730, 1.750000000000000000, 43.04214087805580391 ) ) ;
#15311=AXIS2_PLACEMENT_3D ( 'NONE', #948, #3340, #12698 ) ;
#15332=COLOUR_RGB('Light Blue', 0.31764706, 0.68627451, 0.89019608);
#15333=FILL_AREA_STYLE_COLOUR('',#15332);
#15334=FILL_AREA_STYLE('',(#15333));
#15335=SURFACE_STYLE_FILL_AREA(#15334);
#15336=SURFACE_SIDE_STYLE('',(#15335));
#15337=SURFACE_STYLE_USAGE(.BOTH.,#15336);
#15338=PRESENTATION_STYLE_ASSIGNMENT((#15337));
#15371=STYLED_ITEM('',(#15338),#12454);
#15372=MECHANICAL_DESIGN_GEOMETRIC_PRESENTATION_REPRESENTATION('',(#15371),#12893);
ENDSEC;
END-ISO-10303-21;
